ISO-10303-21;
HEADER;
/* Generated by software containing ST-Developer
 * from STEP Tools, Inc. (www.steptools.com) 
 */

FILE_DESCRIPTION(
/* description */ ('Bearing friction torque test rig'),
/* implementation_level */ '2;1');

FILE_NAME(
/* name */ 'Support inner spacer (1).step',
/* time_stamp */ '2026-10-28T03:24:04-07:00',
/* author */ (''),
/* organization */ (''),
/* preprocessor_version */ 'ST-DEVELOPER v20.2',
/* originating_system */ 'Autodesk Translation Framework v15.17.0.0',
/* authorisation */ '');

FILE_SCHEMA (('AUTOMOTIVE_DESIGN { 1 0 10303 214 3 1 1 }'));
ENDSEC;

DATA;
#10=MECHANICAL_DESIGN_GEOMETRIC_PRESENTATION_REPRESENTATION('',(#584),#14822);
#491=SHAPE_REPRESENTATION_RELATIONSHIP('SRR','None',#15033,#530);
#530=ADVANCED_BREP_SHAPE_REPRESENTATION('',(#635),#14813);
#584=STYLED_ITEM('',(#15298),#635);
#635=MANIFOLD_SOLID_BREP('Body1',#7703);
#838=FACE_BOUND('',#2121,.T.);
#839=FACE_BOUND('',#2123,.T.);
#1063=PLANE('',#9021);
#1064=PLANE('',#9022);
#1479=FACE_OUTER_BOUND('',#2118,.T.);
#1480=FACE_OUTER_BOUND('',#2119,.T.);
#1481=FACE_OUTER_BOUND('',#2120,.T.);
#1482=FACE_OUTER_BOUND('',#2122,.T.);
#2118=EDGE_LOOP('',(#6768,#6769,#6770,#6771));
#2119=EDGE_LOOP('',(#6772,#6773,#6774,#6775));
#2120=EDGE_LOOP('',(#6776));
#2121=EDGE_LOOP('',(#6777));
#2122=EDGE_LOOP('',(#6778));
#2123=EDGE_LOOP('',(#6779));
#2606=LINE('',#14140,#3050);
#2607=LINE('',#14146,#3051);
#3050=VECTOR('',#11303,0.605);
#3051=VECTOR('',#11310,0.9);
#3492=CIRCLE('',#9016,0.605);
#3493=CIRCLE('',#9017,0.605);
#3494=CIRCLE('',#9019,0.9);
#3495=CIRCLE('',#9020,0.9);
#4107=VERTEX_POINT('',#14137);
#4108=VERTEX_POINT('',#14139);
#4109=VERTEX_POINT('',#14143);
#4110=VERTEX_POINT('',#14145);
#5010=EDGE_CURVE('',#4107,#4107,#3492,.T.);
#5011=EDGE_CURVE('',#4107,#4108,#2606,.T.);
#5012=EDGE_CURVE('',#4108,#4108,#3493,.T.);
#5013=EDGE_CURVE('',#4109,#4109,#3494,.T.);
#5014=EDGE_CURVE('',#4109,#4110,#2607,.T.);
#5015=EDGE_CURVE('',#4110,#4110,#3495,.T.);
#6768=ORIENTED_EDGE('',*,*,#5010,.F.);
#6769=ORIENTED_EDGE('',*,*,#5011,.T.);
#6770=ORIENTED_EDGE('',*,*,#5012,.T.);
#6771=ORIENTED_EDGE('',*,*,#5011,.F.);
#6772=ORIENTED_EDGE('',*,*,#5013,.F.);
#6773=ORIENTED_EDGE('',*,*,#5014,.T.);
#6774=ORIENTED_EDGE('',*,*,#5015,.T.);
#6775=ORIENTED_EDGE('',*,*,#5014,.F.);
#6776=ORIENTED_EDGE('',*,*,#5013,.T.);
#6777=ORIENTED_EDGE('',*,*,#5010,.T.);
#6778=ORIENTED_EDGE('',*,*,#5015,.F.);
#6779=ORIENTED_EDGE('',*,*,#5012,.F.);
#7183=CYLINDRICAL_SURFACE('',#9015,0.605);
#7184=CYLINDRICAL_SURFACE('',#9018,0.9);
#7590=ADVANCED_FACE('',(#1479),#7183,.F.);
#7591=ADVANCED_FACE('',(#1480),#7184,.T.);
#7592=ADVANCED_FACE('',(#1481,#838),#1063,.T.);
#7593=ADVANCED_FACE('',(#1482,#839),#1064,.F.);
#7703=CLOSED_SHELL('',(#7590,#7591,#7592,#7593));
#9014=AXIS2_PLACEMENT_3D('',#14135,#11297,#11298);
#9015=AXIS2_PLACEMENT_3D('',#14136,#11299,#11300);
#9016=AXIS2_PLACEMENT_3D('',#14138,#11301,#11302);
#9017=AXIS2_PLACEMENT_3D('',#14141,#11304,#11305);
#9018=AXIS2_PLACEMENT_3D('',#14142,#11306,#11307);
#9019=AXIS2_PLACEMENT_3D('',#14144,#11308,#11309);
#9020=AXIS2_PLACEMENT_3D('',#14147,#11311,#11312);
#9021=AXIS2_PLACEMENT_3D('',#14148,#11313,#11314);
#9022=AXIS2_PLACEMENT_3D('',#14149,#11315,#11316);
#11297=DIRECTION('axis',(0.,0.,1.));
#11298=DIRECTION('refdir',(1.,0.,0.));
#11299=DIRECTION('center_axis',(0.,1.,0.));
#11300=DIRECTION('ref_axis',(1.,0.,0.));
#11301=DIRECTION('center_axis',(0.,-1.,0.));
#11302=DIRECTION('ref_axis',(1.,0.,0.));
#11303=DIRECTION('',(0.,-1.,0.));
#11304=DIRECTION('center_axis',(0.,-1.,0.));
#11305=DIRECTION('ref_axis',(1.,0.,0.));
#11306=DIRECTION('center_axis',(0.,1.,0.));
#11307=DIRECTION('ref_axis',(1.,0.,0.));
#11308=DIRECTION('center_axis',(0.,1.,0.));
#11309=DIRECTION('ref_axis',(1.,0.,0.));
#11310=DIRECTION('',(0.,-1.,0.));
#11311=DIRECTION('center_axis',(0.,1.,0.));
#11312=DIRECTION('ref_axis',(1.,0.,0.));
#11313=DIRECTION('center_axis',(0.,1.,0.));
#11314=DIRECTION('ref_axis',(1.,0.,0.));
#11315=DIRECTION('center_axis',(0.,1.,0.));
#11316=DIRECTION('ref_axis',(1.,0.,0.));
#14135=CARTESIAN_POINT('',(0.,0.,0.));
#14136=CARTESIAN_POINT('Origin',(0.,2.5,7.));
#14137=CARTESIAN_POINT('',(-0.605,6.5,7.));
#14138=CARTESIAN_POINT('Origin',(0.,6.5,7.));
#14139=CARTESIAN_POINT('',(-0.605,2.5,7.));
#14140=CARTESIAN_POINT('',(-0.605,2.5,7.));
#14141=CARTESIAN_POINT('Origin',(0.,2.5,7.));
#14142=CARTESIAN_POINT('Origin',(0.,2.5,7.));
#14143=CARTESIAN_POINT('',(-0.9,6.5,7.));
#14144=CARTESIAN_POINT('Origin',(0.,6.5,7.));
#14145=CARTESIAN_POINT('',(-0.9,2.5,7.));
#14146=CARTESIAN_POINT('',(-0.9,2.5,7.));
#14147=CARTESIAN_POINT('Origin',(0.,2.5,7.));
#14148=CARTESIAN_POINT('Origin',(0.,6.5,7.));
#14149=CARTESIAN_POINT('Origin',(0.,2.5,7.));
#14768=UNCERTAINTY_MEASURE_WITH_UNIT(LENGTH_MEASURE(0.001),#14823,
'DISTANCE_ACCURACY_VALUE',
'Maximum model space distance between geometric entities at asserted c
onnectivities');
#14777=UNCERTAINTY_MEASURE_WITH_UNIT(LENGTH_MEASURE(0.001),#14823,
'DISTANCE_ACCURACY_VALUE',
'Maximum model space distance between geometric entities at asserted c
onnectivities');
#14813=(
GEOMETRIC_REPRESENTATION_CONTEXT(3)
GLOBAL_UNCERTAINTY_ASSIGNED_CONTEXT((#14768))
GLOBAL_UNIT_ASSIGNED_CONTEXT((#14823,#14825,#14826))
REPRESENTATION_CONTEXT('','3D')
);
#14822=(
GEOMETRIC_REPRESENTATION_CONTEXT(3)
GLOBAL_UNCERTAINTY_ASSIGNED_CONTEXT((#14777))
GLOBAL_UNIT_ASSIGNED_CONTEXT((#14823,#14825,#14826))
REPRESENTATION_CONTEXT('','3D')
);
#14823=(
LENGTH_UNIT()
NAMED_UNIT(*)
SI_UNIT(.CENTI.,.METRE.)
);
#14825=(
NAMED_UNIT(*)
PLANE_ANGLE_UNIT()
SI_UNIT($,.RADIAN.)
);
#14826=(
NAMED_UNIT(*)
SI_UNIT($,.STERADIAN.)
SOLID_ANGLE_UNIT()
);
#14862=SHAPE_DEFINITION_REPRESENTATION(#14972,#15033);
#14972=PRODUCT_DEFINITION_SHAPE('',$,#15078);
#15033=SHAPE_REPRESENTATION('',(#9014),#14813);
#15042=PRODUCT_DEFINITION_CONTEXT('part definition',#15176,'design');
#15078=PRODUCT_DEFINITION('Support inner spacer (1)',
'Support inner spacer (1)',#15122,#15042);
#15122=PRODUCT_DEFINITION_FORMATION('',$,#15213);
#15176=APPLICATION_CONTEXT(
'Core Data for Automotive Mechanical Design Process');
#15177=PRODUCT_CONTEXT('part definition',#15176,'mechanical');
#15213=PRODUCT('Support inner spacer (1)','Support inner spacer (1)',
'Support inner spacer (1)',(#15177));
#15292=COLOUR_RGB('Off White',0.89,0.88,0.83);
#15293=FILL_AREA_STYLE_COLOUR('',#15292);
#15294=FILL_AREA_STYLE('',(#15293));
#15295=SURFACE_STYLE_FILL_AREA(#15294);
#15296=SURFACE_SIDE_STYLE('',(#15295));
#15297=SURFACE_STYLE_USAGE(.BOTH.,#15296);
#15298=PRESENTATION_STYLE_ASSIGNMENT((#15297));
ENDSEC;
END-ISO-10303-21;
